ISO-10303-21;
HEADER;
/* Generated by software containing ST-Developer
 * from STEP Tools, Inc. (www.steptools.com) 
 */

FILE_DESCRIPTION(
/* description */ (''),
/* implementation_level */ '2;1');

FILE_NAME(
/* name */ '10_Barrel_Key_DIN_6885_6x6x40.step',
/* time_stamp */ '2026-10-26T07:49:00-07:00',
/* author */ (''),
/* organization */ (''),
/* preprocessor_version */ 'ST-DEVELOPER v20.2',
/* originating_system */ 'Autodesk Translation Framework v15.15.0.0',
/* authorisation */ '');

FILE_SCHEMA (('AUTOMOTIVE_DESIGN { 1 0 10303 214 3 1 1 }'));
ENDSEC;

DATA;
#10=MECHANICAL_DESIGN_GEOMETRIC_PRESENTATION_REPRESENTATION('',(#183),#38507);
#153=SHAPE_REPRESENTATION_RELATIONSHIP('SRR','None',#38581,#168);
#168=ADVANCED_BREP_SHAPE_REPRESENTATION('',(#198),#38498);
#183=STYLED_ITEM('',(#38720),#198);
#198=MANIFOLD_SOLID_BREP('Body1',#15077);
#768=PLANE('',#16153);
#769=PLANE('',#16154);
#770=PLANE('',#16155);
#771=PLANE('',#16156);
#772=PLANE('',#16157);
#773=PLANE('',#16158);
#774=PLANE('',#16159);
#775=PLANE('',#16160);
#776=PLANE('',#16161);
#777=PLANE('',#16162);
#778=PLANE('',#16163);
#779=PLANE('',#16164);
#780=PLANE('',#16165);
#781=PLANE('',#16166);
#782=PLANE('',#16167);
#783=PLANE('',#16168);
#784=PLANE('',#16169);
#785=PLANE('',#16170);
#2113=FACE_OUTER_BOUND('',#3074,.T.);
#2114=FACE_OUTER_BOUND('',#3075,.T.);
#2115=FACE_OUTER_BOUND('',#3076,.T.);
#2116=FACE_OUTER_BOUND('',#3077,.T.);
#2117=FACE_OUTER_BOUND('',#3078,.T.);
#2118=FACE_OUTER_BOUND('',#3079,.T.);
#2119=FACE_OUTER_BOUND('',#3080,.T.);
#2120=FACE_OUTER_BOUND('',#3081,.T.);
#2121=FACE_OUTER_BOUND('',#3082,.T.);
#2122=FACE_OUTER_BOUND('',#3083,.T.);
#2123=FACE_OUTER_BOUND('',#3084,.T.);
#2124=FACE_OUTER_BOUND('',#3085,.T.);
#2125=FACE_OUTER_BOUND('',#3086,.T.);
#2126=FACE_OUTER_BOUND('',#3087,.T.);
#2127=FACE_OUTER_BOUND('',#3088,.T.);
#2128=FACE_OUTER_BOUND('',#3089,.T.);
#2129=FACE_OUTER_BOUND('',#3090,.T.);
#2130=FACE_OUTER_BOUND('',#3091,.T.);
#3074=EDGE_LOOP('',(#12261,#12262,#12263,#12264,#12265,#12266));
#3075=EDGE_LOOP('',(#12267,#12268,#12269,#12270));
#3076=EDGE_LOOP('',(#12271,#12272,#12273,#12274,#12275,#12276));
#3077=EDGE_LOOP('',(#12277,#12278,#12279,#12280,#12281,#12282));
#3078=EDGE_LOOP('',(#12283,#12284,#12285,#12286,#12287,#12288));
#3079=EDGE_LOOP('',(#12289,#12290,#12291,#12292));
#3080=EDGE_LOOP('',(#12293,#12294,#12295,#12296,#12297,#12298));
#3081=EDGE_LOOP('',(#12299,#12300,#12301,#12302,#12303,#12304));
#3082=EDGE_LOOP('',(#12305,#12306,#12307,#12308));
#3083=EDGE_LOOP('',(#12309,#12310,#12311,#12312,#12313,#12314));
#3084=EDGE_LOOP('',(#12315,#12316,#12317,#12318,#12319,#12320));
#3085=EDGE_LOOP('',(#12321,#12322,#12323,#12324));
#3086=EDGE_LOOP('',(#12325,#12326,#12327,#12328,#12329,#12330));
#3087=EDGE_LOOP('',(#12331,#12332,#12333,#12334,#12335,#12336));
#3088=EDGE_LOOP('',(#12337,#12338,#12339,#12340,#12341,#12342));
#3089=EDGE_LOOP('',(#12343,#12344,#12345,#12346));
#3090=EDGE_LOOP('',(#12347,#12348,#12349,#12350,#12351,#12352));
#3091=EDGE_LOOP('',(#12353,#12354,#12355,#12356));
#4058=LINE('',#26750,#5127);
#4059=LINE('',#26752,#5128);
#4060=LINE('',#26754,#5129);
#4061=LINE('',#26756,#5130);
#4062=LINE('',#26758,#5131);
#4063=LINE('',#26759,#5132);
#4064=LINE('',#26762,#5133);
#4065=LINE('',#26764,#5134);
#4066=LINE('',#26765,#5135);
#4067=LINE('',#26768,#5136);
#4068=LINE('',#26770,#5137);
#4069=LINE('',#26772,#5138);
#4070=LINE('',#26773,#5139);
#4071=LINE('',#26776,#5140);
#4072=LINE('',#26778,#5141);
#4073=LINE('',#26780,#5142);
#4074=LINE('',#26781,#5143);
#4075=LINE('',#26785,#5144);
#4076=LINE('',#26787,#5145);
#4077=LINE('',#26788,#5146);
#4078=LINE('',#26790,#5147);
#4079=LINE('',#26791,#5148);
#4080=LINE('',#26794,#5149);
#4081=LINE('',#26796,#5150);
#4082=LINE('',#26797,#5151);
#4083=LINE('',#26800,#5152);
#4084=LINE('',#26802,#5153);
#4085=LINE('',#26804,#5154);
#4086=LINE('',#26805,#5155);
#4087=LINE('',#26808,#5156);
#4088=LINE('',#26809,#5157);
#4089=LINE('',#26810,#5158);
#4090=LINE('',#26813,#5159);
#4091=LINE('',#26814,#5160);
#4092=LINE('',#26817,#5161);
#4093=LINE('',#26819,#5162);
#4094=LINE('',#26821,#5163);
#4095=LINE('',#26822,#5164);
#4096=LINE('',#26825,#5165);
#4097=LINE('',#26826,#5166);
#4098=LINE('',#26827,#5167);
#4099=LINE('',#26830,#5168);
#4100=LINE('',#26831,#5169);
#4101=LINE('',#26834,#5170);
#4102=LINE('',#26836,#5171);
#4103=LINE('',#26837,#5172);
#4104=LINE('',#26839,#5173);
#4105=LINE('',#26841,#5174);
#5127=VECTOR('',#19105,10.);
#5128=VECTOR('',#19106,10.);
#5129=VECTOR('',#19107,10.);
#5130=VECTOR('',#19108,10.);
#5131=VECTOR('',#19109,10.);
#5132=VECTOR('',#19110,10.);
#5133=VECTOR('',#19113,10.);
#5134=VECTOR('',#19114,10.);
#5135=VECTOR('',#19115,10.);
#5136=VECTOR('',#19118,10.);
#5137=VECTOR('',#19119,10.);
#5138=VECTOR('',#19120,10.);
#5139=VECTOR('',#19121,10.);
#5140=VECTOR('',#19124,10.);
#5141=VECTOR('',#19125,10.);
#5142=VECTOR('',#19126,10.);
#5143=VECTOR('',#19127,10.);
#5144=VECTOR('',#19130,10.);
#5145=VECTOR('',#19131,10.);
#5146=VECTOR('',#19132,10.);
#5147=VECTOR('',#19133,10.);
#5148=VECTOR('',#19134,10.);
#5149=VECTOR('',#19137,10.);
#5150=VECTOR('',#19138,10.);
#5151=VECTOR('',#19139,10.);
#5152=VECTOR('',#19142,10.);
#5153=VECTOR('',#19143,10.);
#5154=VECTOR('',#19144,10.);
#5155=VECTOR('',#19145,10.);
#5156=VECTOR('',#19148,10.);
#5157=VECTOR('',#19149,10.);
#5158=VECTOR('',#19150,10.);
#5159=VECTOR('',#19153,10.);
#5160=VECTOR('',#19154,10.);
#5161=VECTOR('',#19157,10.);
#5162=VECTOR('',#19158,10.);
#5163=VECTOR('',#19159,10.);
#5164=VECTOR('',#19160,10.);
#5165=VECTOR('',#19163,10.);
#5166=VECTOR('',#19164,10.);
#5167=VECTOR('',#19165,10.);
#5168=VECTOR('',#19168,10.);
#5169=VECTOR('',#19169,10.);
#5170=VECTOR('',#19172,10.);
#5171=VECTOR('',#19173,10.);
#5172=VECTOR('',#19174,10.);
#5173=VECTOR('',#19177,10.);
#5174=VECTOR('',#19180,10.);
#7046=VERTEX_POINT('',#26748);
#7047=VERTEX_POINT('',#26749);
#7048=VERTEX_POINT('',#26751);
#7049=VERTEX_POINT('',#26753);
#7050=VERTEX_POINT('',#26755);
#7051=VERTEX_POINT('',#26757);
#7052=VERTEX_POINT('',#26761);
#7053=VERTEX_POINT('',#26763);
#7054=VERTEX_POINT('',#26767);
#7055=VERTEX_POINT('',#26769);
#7056=VERTEX_POINT('',#26771);
#7057=VERTEX_POINT('',#26775);
#7058=VERTEX_POINT('',#26777);
#7059=VERTEX_POINT('',#26779);
#7060=VERTEX_POINT('',#26783);
#7061=VERTEX_POINT('',#26784);
#7062=VERTEX_POINT('',#26786);
#7063=VERTEX_POINT('',#26789);
#7064=VERTEX_POINT('',#26793);
#7065=VERTEX_POINT('',#26795);
#7066=VERTEX_POINT('',#26799);
#7067=VERTEX_POINT('',#26801);
#7068=VERTEX_POINT('',#26803);
#7069=VERTEX_POINT('',#26807);
#7070=VERTEX_POINT('',#26812);
#7071=VERTEX_POINT('',#26816);
#7072=VERTEX_POINT('',#26818);
#7073=VERTEX_POINT('',#26820);
#7074=VERTEX_POINT('',#26824);
#7075=VERTEX_POINT('',#26829);
#7076=VERTEX_POINT('',#26833);
#7077=VERTEX_POINT('',#26835);
#8879=EDGE_CURVE('',#7046,#7047,#4058,.T.);
#8880=EDGE_CURVE('',#7047,#7048,#4059,.T.);
#8881=EDGE_CURVE('',#7048,#7049,#4060,.T.);
#8882=EDGE_CURVE('',#7049,#7050,#4061,.T.);
#8883=EDGE_CURVE('',#7050,#7051,#4062,.T.);
#8884=EDGE_CURVE('',#7051,#7046,#4063,.T.);
#8885=EDGE_CURVE('',#7052,#7047,#4064,.T.);
#8886=EDGE_CURVE('',#7053,#7052,#4065,.T.);
#8887=EDGE_CURVE('',#7048,#7053,#4066,.T.);
#8888=EDGE_CURVE('',#7054,#7046,#4067,.T.);
#8889=EDGE_CURVE('',#7054,#7055,#4068,.T.);
#8890=EDGE_CURVE('',#7056,#7055,#4069,.T.);
#8891=EDGE_CURVE('',#7052,#7056,#4070,.T.);
#8892=EDGE_CURVE('',#7051,#7057,#4071,.T.);
#8893=EDGE_CURVE('',#7058,#7057,#4072,.T.);
#8894=EDGE_CURVE('',#7058,#7059,#4073,.T.);
#8895=EDGE_CURVE('',#7059,#7054,#4074,.T.);
#8896=EDGE_CURVE('',#7060,#7061,#4075,.T.);
#8897=EDGE_CURVE('',#7061,#7062,#4076,.T.);
#8898=EDGE_CURVE('',#7062,#7058,#4077,.T.);
#8899=EDGE_CURVE('',#7057,#7063,#4078,.T.);
#8900=EDGE_CURVE('',#7063,#7060,#4079,.T.);
#8901=EDGE_CURVE('',#7064,#7061,#4080,.T.);
#8902=EDGE_CURVE('',#7065,#7064,#4081,.T.);
#8903=EDGE_CURVE('',#7062,#7065,#4082,.T.);
#8904=EDGE_CURVE('',#7066,#7060,#4083,.T.);
#8905=EDGE_CURVE('',#7066,#7067,#4084,.T.);
#8906=EDGE_CURVE('',#7068,#7067,#4085,.T.);
#8907=EDGE_CURVE('',#7064,#7068,#4086,.T.);
#8908=EDGE_CURVE('',#7049,#7069,#4087,.T.);
#8909=EDGE_CURVE('',#7069,#7066,#4088,.T.);
#8910=EDGE_CURVE('',#7063,#7050,#4089,.T.);
#8911=EDGE_CURVE('',#7070,#7059,#4090,.T.);
#8912=EDGE_CURVE('',#7055,#7070,#4091,.T.);
#8913=EDGE_CURVE('',#7068,#7071,#4092,.T.);
#8914=EDGE_CURVE('',#7071,#7072,#4093,.T.);
#8915=EDGE_CURVE('',#7072,#7073,#4094,.T.);
#8916=EDGE_CURVE('',#7073,#7065,#4095,.T.);
#8917=EDGE_CURVE('',#7072,#7074,#4096,.T.);
#8918=EDGE_CURVE('',#7074,#7056,#4097,.T.);
#8919=EDGE_CURVE('',#7070,#7073,#4098,.T.);
#8920=EDGE_CURVE('',#7075,#7071,#4099,.T.);
#8921=EDGE_CURVE('',#7074,#7075,#4100,.T.);
#8922=EDGE_CURVE('',#7067,#7076,#4101,.T.);
#8923=EDGE_CURVE('',#7076,#7077,#4102,.T.);
#8924=EDGE_CURVE('',#7075,#7077,#4103,.T.);
#8925=EDGE_CURVE('',#7077,#7053,#4104,.T.);
#8926=EDGE_CURVE('',#7076,#7069,#4105,.T.);
#12261=ORIENTED_EDGE('',*,*,#8879,.T.);
#12262=ORIENTED_EDGE('',*,*,#8880,.T.);
#12263=ORIENTED_EDGE('',*,*,#8881,.T.);
#12264=ORIENTED_EDGE('',*,*,#8882,.T.);
#12265=ORIENTED_EDGE('',*,*,#8883,.T.);
#12266=ORIENTED_EDGE('',*,*,#8884,.T.);
#12267=ORIENTED_EDGE('',*,*,#8880,.F.);
#12268=ORIENTED_EDGE('',*,*,#8885,.F.);
#12269=ORIENTED_EDGE('',*,*,#8886,.F.);
#12270=ORIENTED_EDGE('',*,*,#8887,.F.);
#12271=ORIENTED_EDGE('',*,*,#8879,.F.);
#12272=ORIENTED_EDGE('',*,*,#8888,.F.);
#12273=ORIENTED_EDGE('',*,*,#8889,.T.);
#12274=ORIENTED_EDGE('',*,*,#8890,.F.);
#12275=ORIENTED_EDGE('',*,*,#8891,.F.);
#12276=ORIENTED_EDGE('',*,*,#8885,.T.);
#12277=ORIENTED_EDGE('',*,*,#8884,.F.);
#12278=ORIENTED_EDGE('',*,*,#8892,.T.);
#12279=ORIENTED_EDGE('',*,*,#8893,.F.);
#12280=ORIENTED_EDGE('',*,*,#8894,.T.);
#12281=ORIENTED_EDGE('',*,*,#8895,.T.);
#12282=ORIENTED_EDGE('',*,*,#8888,.T.);
#12283=ORIENTED_EDGE('',*,*,#8896,.T.);
#12284=ORIENTED_EDGE('',*,*,#8897,.T.);
#12285=ORIENTED_EDGE('',*,*,#8898,.T.);
#12286=ORIENTED_EDGE('',*,*,#8893,.T.);
#12287=ORIENTED_EDGE('',*,*,#8899,.T.);
#12288=ORIENTED_EDGE('',*,*,#8900,.T.);
#12289=ORIENTED_EDGE('',*,*,#8897,.F.);
#12290=ORIENTED_EDGE('',*,*,#8901,.F.);
#12291=ORIENTED_EDGE('',*,*,#8902,.F.);
#12292=ORIENTED_EDGE('',*,*,#8903,.F.);
#12293=ORIENTED_EDGE('',*,*,#8896,.F.);
#12294=ORIENTED_EDGE('',*,*,#8904,.F.);
#12295=ORIENTED_EDGE('',*,*,#8905,.T.);
#12296=ORIENTED_EDGE('',*,*,#8906,.F.);
#12297=ORIENTED_EDGE('',*,*,#8907,.F.);
#12298=ORIENTED_EDGE('',*,*,#8901,.T.);
#12299=ORIENTED_EDGE('',*,*,#8882,.F.);
#12300=ORIENTED_EDGE('',*,*,#8908,.T.);
#12301=ORIENTED_EDGE('',*,*,#8909,.T.);
#12302=ORIENTED_EDGE('',*,*,#8904,.T.);
#12303=ORIENTED_EDGE('',*,*,#8900,.F.);
#12304=ORIENTED_EDGE('',*,*,#8910,.T.);
#12305=ORIENTED_EDGE('',*,*,#8895,.F.);
#12306=ORIENTED_EDGE('',*,*,#8911,.F.);
#12307=ORIENTED_EDGE('',*,*,#8912,.F.);
#12308=ORIENTED_EDGE('',*,*,#8889,.F.);
#12309=ORIENTED_EDGE('',*,*,#8913,.T.);
#12310=ORIENTED_EDGE('',*,*,#8914,.T.);
#12311=ORIENTED_EDGE('',*,*,#8915,.T.);
#12312=ORIENTED_EDGE('',*,*,#8916,.T.);
#12313=ORIENTED_EDGE('',*,*,#8902,.T.);
#12314=ORIENTED_EDGE('',*,*,#8907,.T.);
#12315=ORIENTED_EDGE('',*,*,#8915,.F.);
#12316=ORIENTED_EDGE('',*,*,#8917,.T.);
#12317=ORIENTED_EDGE('',*,*,#8918,.T.);
#12318=ORIENTED_EDGE('',*,*,#8890,.T.);
#12319=ORIENTED_EDGE('',*,*,#8912,.T.);
#12320=ORIENTED_EDGE('',*,*,#8919,.T.);
#12321=ORIENTED_EDGE('',*,*,#8914,.F.);
#12322=ORIENTED_EDGE('',*,*,#8920,.F.);
#12323=ORIENTED_EDGE('',*,*,#8921,.F.);
#12324=ORIENTED_EDGE('',*,*,#8917,.F.);
#12325=ORIENTED_EDGE('',*,*,#8913,.F.);
#12326=ORIENTED_EDGE('',*,*,#8906,.T.);
#12327=ORIENTED_EDGE('',*,*,#8922,.T.);
#12328=ORIENTED_EDGE('',*,*,#8923,.T.);
#12329=ORIENTED_EDGE('',*,*,#8924,.F.);
#12330=ORIENTED_EDGE('',*,*,#8920,.T.);
#12331=ORIENTED_EDGE('',*,*,#8918,.F.);
#12332=ORIENTED_EDGE('',*,*,#8921,.T.);
#12333=ORIENTED_EDGE('',*,*,#8924,.T.);
#12334=ORIENTED_EDGE('',*,*,#8925,.T.);
#12335=ORIENTED_EDGE('',*,*,#8886,.T.);
#12336=ORIENTED_EDGE('',*,*,#8891,.T.);
#12337=ORIENTED_EDGE('',*,*,#8881,.F.);
#12338=ORIENTED_EDGE('',*,*,#8887,.T.);
#12339=ORIENTED_EDGE('',*,*,#8925,.F.);
#12340=ORIENTED_EDGE('',*,*,#8923,.F.);
#12341=ORIENTED_EDGE('',*,*,#8926,.T.);
#12342=ORIENTED_EDGE('',*,*,#8908,.F.);
#12343=ORIENTED_EDGE('',*,*,#8909,.F.);
#12344=ORIENTED_EDGE('',*,*,#8926,.F.);
#12345=ORIENTED_EDGE('',*,*,#8922,.F.);
#12346=ORIENTED_EDGE('',*,*,#8905,.F.);
#12347=ORIENTED_EDGE('',*,*,#8898,.F.);
#12348=ORIENTED_EDGE('',*,*,#8903,.T.);
#12349=ORIENTED_EDGE('',*,*,#8916,.F.);
#12350=ORIENTED_EDGE('',*,*,#8919,.F.);
#12351=ORIENTED_EDGE('',*,*,#8911,.T.);
#12352=ORIENTED_EDGE('',*,*,#8894,.F.);
#12353=ORIENTED_EDGE('',*,*,#8883,.F.);
#12354=ORIENTED_EDGE('',*,*,#8910,.F.);
#12355=ORIENTED_EDGE('',*,*,#8899,.F.);
#12356=ORIENTED_EDGE('',*,*,#8892,.F.);
#14680=ADVANCED_FACE('',(#2113),#768,.T.);
#14681=ADVANCED_FACE('',(#2114),#769,.T.);
#14682=ADVANCED_FACE('',(#2115),#770,.T.);
#14683=ADVANCED_FACE('',(#2116),#771,.T.);
#14684=ADVANCED_FACE('',(#2117),#772,.T.);
#14685=ADVANCED_FACE('',(#2118),#773,.T.);
#14686=ADVANCED_FACE('',(#2119),#774,.T.);
#14687=ADVANCED_FACE('',(#2120),#775,.T.);
#14688=ADVANCED_FACE('',(#2121),#776,.T.);
#14689=ADVANCED_FACE('',(#2122),#777,.T.);
#14690=ADVANCED_FACE('',(#2123),#778,.T.);
#14691=ADVANCED_FACE('',(#2124),#779,.T.);
#14692=ADVANCED_FACE('',(#2125),#780,.T.);
#14693=ADVANCED_FACE('',(#2126),#781,.T.);
#14694=ADVANCED_FACE('',(#2127),#782,.T.);
#14695=ADVANCED_FACE('',(#2128),#783,.T.);
#14696=ADVANCED_FACE('',(#2129),#784,.T.);
#14697=ADVANCED_FACE('',(#2130),#785,.F.);
#15077=CLOSED_SHELL('',(#14680,#14681,#14682,#14683,#14684,#14685,#14686,
#14687,#14688,#14689,#14690,#14691,#14692,#14693,#14694,#14695,#14696,#14697));
#16152=AXIS2_PLACEMENT_3D('',#26746,#19101,#19102);
#16153=AXIS2_PLACEMENT_3D('',#26747,#19103,#19104);
#16154=AXIS2_PLACEMENT_3D('',#26760,#19111,#19112);
#16155=AXIS2_PLACEMENT_3D('',#26766,#19116,#19117);
#16156=AXIS2_PLACEMENT_3D('',#26774,#19122,#19123);
#16157=AXIS2_PLACEMENT_3D('',#26782,#19128,#19129);
#16158=AXIS2_PLACEMENT_3D('',#26792,#19135,#19136);
#16159=AXIS2_PLACEMENT_3D('',#26798,#19140,#19141);
#16160=AXIS2_PLACEMENT_3D('',#26806,#19146,#19147);
#16161=AXIS2_PLACEMENT_3D('',#26811,#19151,#19152);
#16162=AXIS2_PLACEMENT_3D('',#26815,#19155,#19156);
#16163=AXIS2_PLACEMENT_3D('',#26823,#19161,#19162);
#16164=AXIS2_PLACEMENT_3D('',#26828,#19166,#19167);
#16165=AXIS2_PLACEMENT_3D('',#26832,#19170,#19171);
#16166=AXIS2_PLACEMENT_3D('',#26838,#19175,#19176);
#16167=AXIS2_PLACEMENT_3D('',#26840,#19178,#19179);
#16168=AXIS2_PLACEMENT_3D('',#26842,#19181,#19182);
#16169=AXIS2_PLACEMENT_3D('',#26843,#19183,#19184);
#16170=AXIS2_PLACEMENT_3D('',#26844,#19185,#19186);
#19101=DIRECTION('axis',(0.,0.,1.));
#19102=DIRECTION('refdir',(1.,0.,0.));
#19103=DIRECTION('center_axis',(-0.707106781186546,0.,-0.707106781186549));
#19104=DIRECTION('ref_axis',(-0.707106781186549,0.,0.707106781186546));
#19105=DIRECTION('',(0.577350269189628,-0.577350269189625,-0.577350269189625));
#19106=DIRECTION('',(0.,-1.,0.));
#19107=DIRECTION('',(-0.577350269189628,-0.577350269189625,0.577350269189625));
#19108=DIRECTION('',(-0.577350269189627,0.577350269189627,0.577350269189624));
#19109=DIRECTION('',(0.,1.,0.));
#19110=DIRECTION('',(0.577350269189627,0.577350269189627,-0.577350269189624));
#19111=DIRECTION('center_axis',(0.,0.,-1.));
#19112=DIRECTION('ref_axis',(0.,1.,0.));
#19113=DIRECTION('',(-1.,0.,0.));
#19114=DIRECTION('',(0.,1.,0.));
#19115=DIRECTION('',(1.,0.,0.));
#19116=DIRECTION('center_axis',(0.,0.707106781186548,-0.707106781186548));
#19117=DIRECTION('ref_axis',(-1.,0.,0.));
#19118=DIRECTION('',(-0.577350269189626,-0.577350269189626,-0.577350269189626));
#19119=DIRECTION('',(1.,0.,0.));
#19120=DIRECTION('',(-0.577350269189611,0.577350269189633,0.577350269189633));
#19121=DIRECTION('',(0.577350269189611,0.577350269189633,0.577350269189633));
#19122=DIRECTION('center_axis',(-0.707106781186548,0.707106781186548,0.));
#19123=DIRECTION('ref_axis',(0.,0.,1.));
#19124=DIRECTION('',(0.,0.,1.));
#19125=DIRECTION('',(-0.577350269189626,-0.577350269189626,-0.577350269189626));
#19126=DIRECTION('',(0.577350269189626,0.577350269189626,-0.577350269189626));
#19127=DIRECTION('',(0.,0.,-1.));
#19128=DIRECTION('center_axis',(-0.707106781186548,0.,0.707106781186548));
#19129=DIRECTION('ref_axis',(0.707106781186548,0.,0.707106781186548));
#19130=DIRECTION('',(0.577350269189627,0.577350269189623,0.577350269189627));
#19131=DIRECTION('',(0.,1.,0.));
#19132=DIRECTION('',(-0.577350269189626,0.577350269189626,-0.577350269189626));
#19133=DIRECTION('',(0.,-1.,0.));
#19134=DIRECTION('',(0.577350269189626,-0.577350269189626,0.577350269189626));
#19135=DIRECTION('center_axis',(0.,0.,1.));
#19136=DIRECTION('ref_axis',(0.,-1.,0.));
#19137=DIRECTION('',(-1.,0.,0.));
#19138=DIRECTION('',(0.,-1.,0.));
#19139=DIRECTION('',(1.,0.,0.));
#19140=DIRECTION('center_axis',(0.,-0.70710678118655,0.707106781186545));
#19141=DIRECTION('ref_axis',(1.,0.,0.));
#19142=DIRECTION('',(-0.577350269189624,0.577350269189624,0.577350269189629));
#19143=DIRECTION('',(1.,0.,0.));
#19144=DIRECTION('',(-0.57735026918961,-0.577350269189632,-0.577350269189636));
#19145=DIRECTION('',(0.577350269189613,-0.57735026918963,-0.577350269189634));
#19146=DIRECTION('center_axis',(-0.707106781186548,-0.707106781186548,0.));
#19147=DIRECTION('ref_axis',(0.,0.,1.));
#19148=DIRECTION('',(0.577350269189626,-0.577350269189626,0.577350269189626));
#19149=DIRECTION('',(0.,0.,1.));
#19150=DIRECTION('',(0.,0.,-1.));
#19151=DIRECTION('center_axis',(0.,1.,0.));
#19152=DIRECTION('ref_axis',(0.,0.,1.));
#19153=DIRECTION('',(-1.,0.,0.));
#19154=DIRECTION('',(0.,0.,1.));
#19155=DIRECTION('center_axis',(0.707106781186561,0.,0.707106781186534));
#19156=DIRECTION('ref_axis',(0.707106781186534,0.,-0.707106781186561));
#19157=DIRECTION('',(0.577350269189611,0.577350269189633,-0.577350269189633));
#19158=DIRECTION('',(0.,1.,0.));
#19159=DIRECTION('',(-0.577350269189611,0.577350269189633,0.577350269189633));
#19160=DIRECTION('',(-0.577350269189611,-0.577350269189633,0.577350269189633));
#19161=DIRECTION('center_axis',(0.707106781186561,0.707106781186534,0.));
#19162=DIRECTION('ref_axis',(0.,0.,-1.));
#19163=DIRECTION('',(0.,0.,-1.));
#19164=DIRECTION('',(-0.577350269189611,0.577350269189633,-0.577350269189633));
#19165=DIRECTION('',(0.577350269189611,-0.577350269189633,0.577350269189633));
#19166=DIRECTION('center_axis',(1.,0.,0.));
#19167=DIRECTION('ref_axis',(0.,0.,-1.));
#19168=DIRECTION('',(0.,0.,1.));
#19169=DIRECTION('',(0.,-1.,0.));
#19170=DIRECTION('center_axis',(0.707106781186561,-0.707106781186534,0.));
#19171=DIRECTION('ref_axis',(0.,0.,-1.));
#19172=DIRECTION('',(0.,0.,-1.));
#19173=DIRECTION('',(0.577350269189611,0.577350269189633,-0.577350269189633));
#19174=DIRECTION('',(-0.577350269189611,-0.577350269189633,-0.577350269189633));
#19175=DIRECTION('center_axis',(0.707106781186561,0.,-0.707106781186534));
#19176=DIRECTION('ref_axis',(-0.707106781186534,0.,-0.707106781186561));
#19177=DIRECTION('',(-0.577350269189611,0.577350269189633,-0.577350269189633));
#19178=DIRECTION('center_axis',(0.,-0.707106781186548,-0.707106781186548));
#19179=DIRECTION('ref_axis',(-1.,0.,0.));
#19180=DIRECTION('',(-1.,0.,0.));
#19181=DIRECTION('center_axis',(0.,-1.,0.));
#19182=DIRECTION('ref_axis',(0.,0.,-1.));
#19183=DIRECTION('center_axis',(0.,0.707106781186548,0.707106781186548));
#19184=DIRECTION('ref_axis',(1.,0.,0.));
#19185=DIRECTION('center_axis',(1.,0.,0.));
#19186=DIRECTION('ref_axis',(0.,0.,-1.));
#26746=CARTESIAN_POINT('',(0.,0.,0.));
#26747=CARTESIAN_POINT('Origin',(75.17,-1.495,9.13));
#26748=CARTESIAN_POINT('',(75.14,2.84,9.16));
#26749=CARTESIAN_POINT('',(75.29,2.69,9.01));
#26750=CARTESIAN_POINT('',(75.8575,2.1225,8.4425));
#26751=CARTESIAN_POINT('',(75.29,-2.69,9.01));
#26752=CARTESIAN_POINT('',(75.29,-1.495,9.01));
#26753=CARTESIAN_POINT('',(75.14,-2.84,9.16));
#26754=CARTESIAN_POINT('',(75.3591666666667,-2.62083333333333,8.94083333333333));
#26755=CARTESIAN_POINT('',(75.05,-2.75,9.25));
#26756=CARTESIAN_POINT('',(74.2120833333333,-1.91208333333334,10.0879166666667));
#26757=CARTESIAN_POINT('',(75.05,2.75,9.25));
#26758=CARTESIAN_POINT('',(75.05,-1.495,9.25));
#26759=CARTESIAN_POINT('',(74.2129166666667,1.91291666666666,10.0870833333333));
#26760=CARTESIAN_POINT('Origin',(75.05,-2.99,9.01));
#26761=CARTESIAN_POINT('',(114.71,2.69,9.01));
#26762=CARTESIAN_POINT('',(75.05,2.69,9.01));
#26763=CARTESIAN_POINT('',(114.71,-2.69,9.01));
#26764=CARTESIAN_POINT('',(114.71,-1.495,9.01));
#26765=CARTESIAN_POINT('',(75.05,-2.69,9.01));
#26766=CARTESIAN_POINT('Origin',(75.05,2.84,9.16));
#26767=CARTESIAN_POINT('',(75.29,2.99,9.31));
#26768=CARTESIAN_POINT('',(75.3595833333333,3.05958333333333,9.37958333333333));
#26769=CARTESIAN_POINT('',(114.71,2.99,9.31));
#26770=CARTESIAN_POINT('',(75.05,2.99,9.31));
#26771=CARTESIAN_POINT('',(114.86,2.84,9.16));
#26772=CARTESIAN_POINT('',(107.990416666667,9.70958333333326,16.0295833333333));
#26773=CARTESIAN_POINT('',(107.4925,-4.52749999999994,1.79250000000006));
#26774=CARTESIAN_POINT('Origin',(75.17,2.87,10.5075));
#26775=CARTESIAN_POINT('',(75.05,2.75,14.76));
#26776=CARTESIAN_POINT('',(75.05,2.75,10.5075));
#26777=CARTESIAN_POINT('',(75.14,2.84,14.85));
#26778=CARTESIAN_POINT('',(74.2120833333333,1.91208333333334,13.9220833333333));
#26779=CARTESIAN_POINT('',(75.29,2.99,14.7));
#26780=CARTESIAN_POINT('',(75.85875,3.55875,14.13125));
#26781=CARTESIAN_POINT('',(75.29,2.99,10.5075));
#26782=CARTESIAN_POINT('Origin',(75.17,1.495,14.88));
#26783=CARTESIAN_POINT('',(75.14,-2.84,14.85));
#26784=CARTESIAN_POINT('',(75.29,-2.69,15.));
#26785=CARTESIAN_POINT('',(75.8575,-2.12250000000001,15.5675));
#26786=CARTESIAN_POINT('',(75.29,2.69,15.));
#26787=CARTESIAN_POINT('',(75.29,1.495,15.));
#26788=CARTESIAN_POINT('',(75.3591666666667,2.62083333333333,15.0691666666667));
#26789=CARTESIAN_POINT('',(75.05,-2.75,14.76));
#26790=CARTESIAN_POINT('',(75.05,1.495,14.76));
#26791=CARTESIAN_POINT('',(74.2129166666667,-1.91291666666667,13.9229166666667));
#26792=CARTESIAN_POINT('Origin',(75.05,2.99,15.));
#26793=CARTESIAN_POINT('',(114.71,-2.69,15.));
#26794=CARTESIAN_POINT('',(75.05,-2.69,15.));
#26795=CARTESIAN_POINT('',(114.71,2.69,15.));
#26796=CARTESIAN_POINT('',(114.71,1.495,15.));
#26797=CARTESIAN_POINT('',(75.05,2.69,15.));
#26798=CARTESIAN_POINT('Origin',(75.05,-2.84,14.85));
#26799=CARTESIAN_POINT('',(75.29,-2.99,14.7));
#26800=CARTESIAN_POINT('',(75.3595833333333,-3.05958333333334,14.6304166666667));
#26801=CARTESIAN_POINT('',(114.71,-2.99,14.7));
#26802=CARTESIAN_POINT('',(75.05,-2.99,14.7));
#26803=CARTESIAN_POINT('',(114.86,-2.84,14.85));
#26804=CARTESIAN_POINT('',(107.990416666667,-9.70958333333323,7.98041666666672));
#26805=CARTESIAN_POINT('',(107.4925,4.52749999999992,22.2175));
#26806=CARTESIAN_POINT('Origin',(75.17,-2.87,13.5025));
#26807=CARTESIAN_POINT('',(75.29,-2.99,9.31));
#26808=CARTESIAN_POINT('',(75.85875,-3.55875,9.87875));
#26809=CARTESIAN_POINT('',(75.29,-2.99,13.5025));
#26810=CARTESIAN_POINT('',(75.05,-2.75,13.5025));
#26811=CARTESIAN_POINT('Origin',(75.05,2.99,9.01));
#26812=CARTESIAN_POINT('',(114.71,2.99,14.7));
#26813=CARTESIAN_POINT('',(75.05,2.99,14.7));
#26814=CARTESIAN_POINT('',(114.71,2.99,10.5075));
#26815=CARTESIAN_POINT('Origin',(114.83,1.495,14.88));
#26816=CARTESIAN_POINT('',(114.95,-2.75,14.76));
#26817=CARTESIAN_POINT('',(115.787083333333,-1.91291666666665,13.9229166666666));
#26818=CARTESIAN_POINT('',(114.95,2.75,14.76));
#26819=CARTESIAN_POINT('',(114.95,1.495,14.76));
#26820=CARTESIAN_POINT('',(114.86,2.84,14.85));
#26821=CARTESIAN_POINT('',(115.787916666667,1.91208333333331,13.9220833333333));
#26822=CARTESIAN_POINT('',(107.990833333334,-4.02916666666659,21.7191666666666));
#26823=CARTESIAN_POINT('Origin',(114.83,2.87,10.5075));
#26824=CARTESIAN_POINT('',(114.95,2.75,9.25));
#26825=CARTESIAN_POINT('',(114.95,2.75,10.5075));
#26826=CARTESIAN_POINT('',(115.787083333333,1.91291666666665,10.0870833333334));
#26827=CARTESIAN_POINT('',(107.49125,10.2087499999999,7.48125000000006));
#26828=CARTESIAN_POINT('Origin',(114.95,0.,12.005));
#26829=CARTESIAN_POINT('',(114.95,-2.75,9.25));
#26830=CARTESIAN_POINT('',(114.95,-2.75,13.5025));
#26831=CARTESIAN_POINT('',(114.95,-1.495,9.25));
#26832=CARTESIAN_POINT('Origin',(114.83,-2.87,13.5025));
#26833=CARTESIAN_POINT('',(114.71,-2.99,9.31));
#26834=CARTESIAN_POINT('',(114.71,-2.99,13.5025));
#26835=CARTESIAN_POINT('',(114.86,-2.84,9.16000000000001));
#26836=CARTESIAN_POINT('',(107.49125,-10.2087499999999,16.5287499999999));
#26837=CARTESIAN_POINT('',(115.787916666667,-1.91208333333331,10.0879166666667));
#26838=CARTESIAN_POINT('Origin',(114.83,-1.495,9.13));
#26839=CARTESIAN_POINT('',(107.990833333334,4.02916666666659,2.29083333333341));
#26840=CARTESIAN_POINT('Origin',(75.05,-2.84,9.16));
#26841=CARTESIAN_POINT('',(75.05,-2.99,9.31));
#26842=CARTESIAN_POINT('Origin',(75.05,-2.99,15.));
#26843=CARTESIAN_POINT('Origin',(75.05,2.84,14.85));
#26844=CARTESIAN_POINT('Origin',(75.05,0.,12.005));
#38481=UNCERTAINTY_MEASURE_WITH_UNIT(LENGTH_MEASURE(0.01),#38508,
'DISTANCE_ACCURACY_VALUE',
'Maximum model space distance between geometric entities at asserted c
onnectivities');
#38490=UNCERTAINTY_MEASURE_WITH_UNIT(LENGTH_MEASURE(0.01),#38508,
'DISTANCE_ACCURACY_VALUE',
'Maximum model space distance between geometric entities at asserted c
onnectivities');
#38498=(
GEOMETRIC_REPRESENTATION_CONTEXT(3)
GLOBAL_UNCERTAINTY_ASSIGNED_CONTEXT((#38481))
GLOBAL_UNIT_ASSIGNED_CONTEXT((#38508,#38510,#38511))
REPRESENTATION_CONTEXT('','3D')
);
#38507=(
GEOMETRIC_REPRESENTATION_CONTEXT(3)
GLOBAL_UNCERTAINTY_ASSIGNED_CONTEXT((#38490))
GLOBAL_UNIT_ASSIGNED_CONTEXT((#38508,#38510,#38511))
REPRESENTATION_CONTEXT('','3D')
);
#38508=(
LENGTH_UNIT()
NAMED_UNIT(*)
SI_UNIT(.MILLI.,.METRE.)
);
#38510=(
NAMED_UNIT(*)
PLANE_ANGLE_UNIT()
SI_UNIT($,.RADIAN.)
);
#38511=(
NAMED_UNIT(*)
SI_UNIT($,.STERADIAN.)
SOLID_ANGLE_UNIT()
);
#38519=SHAPE_DEFINITION_REPRESENTATION(#38535,#38581);
#38535=PRODUCT_DEFINITION_SHAPE('',$,#38598);
#38581=SHAPE_REPRESENTATION('',(#16152),#38498);
#38590=PRODUCT_DEFINITION_CONTEXT('part definition',#38640,'design');
#38598=PRODUCT_DEFINITION('2026-10-26-01-10-53-965',
'10_Barrel_Key_DIN_6885_6x6x40',#38614,#38590);
#38614=PRODUCT_DEFINITION_FORMATION('',$,#38649);
#38640=APPLICATION_CONTEXT(
'Core Data for Automotive Mechanical Design Process');
#38641=PRODUCT_CONTEXT('part definition',#38640,'mechanical');
#38649=PRODUCT('2026-10-26-01-10-53-965',
'10_Barrel_Key_DIN_6885_6x6x40',$,(#38641));
#38714=COLOUR_RGB('Grey',0.48,0.52,0.57);
#38715=FILL_AREA_STYLE_COLOUR('',#38714);
#38716=FILL_AREA_STYLE('',(#38715));
#38717=SURFACE_STYLE_FILL_AREA(#38716);
#38718=SURFACE_SIDE_STYLE('',(#38717));
#38719=SURFACE_STYLE_USAGE(.BOTH.,#38718);
#38720=PRESENTATION_STYLE_ASSIGNMENT((#38719));
ENDSEC;
END-ISO-10303-21;
